ISO-10303-21;
HEADER;
/* Generated by software containing ST-Developer
 * from STEP Tools, Inc. (www.steptools.com) 
 */

FILE_DESCRIPTION(
/* description */ ('Bin tilter linkage'),
/* implementation_level */ '2;1');

FILE_NAME(
/* name */ 'Screw keeper fastener (3).step',
/* time_stamp */ '2026-10-28T03:26:24-07:00',
/* author */ (''),
/* organization */ (''),
/* preprocessor_version */ 'ST-DEVELOPER v20.2',
/* originating_system */ 'Autodesk Translation Framework v15.17.0.0',
/* authorisation */ '');

FILE_SCHEMA (('AUTOMOTIVE_DESIGN { 1 0 10303 214 3 1 1 }'));
ENDSEC;

DATA;
#10=MECHANICAL_DESIGN_GEOMETRIC_PRESENTATION_REPRESENTATION('',(#881),#23728);
#669=SHAPE_REPRESENTATION_RELATIONSHIP('SRR','None',#24133,#775);
#775=ADVANCED_BREP_SHAPE_REPRESENTATION('',(#995),#23633);
#881=STYLED_ITEM('',(#24772),#995);
#995=MANIFOLD_SOLID_BREP('Body1',#12411);
#1202=FACE_BOUND('',#2948,.T.);
#1574=PLANE('',#14029);
#1575=PLANE('',#14034);
#1576=PLANE('',#14037);
#2055=FACE_OUTER_BOUND('',#2947,.T.);
#2056=FACE_OUTER_BOUND('',#2949,.T.);
#2057=FACE_OUTER_BOUND('',#2950,.T.);
#2058=FACE_OUTER_BOUND('',#2951,.T.);
#2059=FACE_OUTER_BOUND('',#2952,.T.);
#2947=EDGE_LOOP('',(#9069));
#2948=EDGE_LOOP('',(#9070));
#2949=EDGE_LOOP('',(#9071,#9072,#9073,#9074));
#2950=EDGE_LOOP('',(#9075));
#2951=EDGE_LOOP('',(#9076,#9077,#9078,#9079));
#2952=EDGE_LOOP('',(#9080));
#4031=LINE('',#20520,#4706);
#4032=LINE('',#20524,#4707);
#4706=VECTOR('',#16372,0.35);
#4707=VECTOR('',#16377,0.2);
#5365=CIRCLE('',#14030,0.35);
#5366=CIRCLE('',#14031,0.2);
#5367=CIRCLE('',#14033,0.35);
#5368=CIRCLE('',#14036,0.2);
#6189=VERTEX_POINT('',#20513);
#6190=VERTEX_POINT('',#20515);
#6191=VERTEX_POINT('',#20518);
#6192=VERTEX_POINT('',#20523);
#7274=EDGE_CURVE('',#6189,#6189,#5365,.T.);
#7275=EDGE_CURVE('',#6190,#6190,#5366,.T.);
#7276=EDGE_CURVE('',#6191,#6191,#5367,.T.);
#7277=EDGE_CURVE('',#6191,#6189,#4031,.T.);
#7278=EDGE_CURVE('',#6190,#6192,#4032,.T.);
#7279=EDGE_CURVE('',#6192,#6192,#5368,.T.);
#9069=ORIENTED_EDGE('',*,*,#7274,.F.);
#9070=ORIENTED_EDGE('',*,*,#7275,.T.);
#9071=ORIENTED_EDGE('',*,*,#7276,.F.);
#9072=ORIENTED_EDGE('',*,*,#7277,.T.);
#9073=ORIENTED_EDGE('',*,*,#7274,.T.);
#9074=ORIENTED_EDGE('',*,*,#7277,.F.);
#9075=ORIENTED_EDGE('',*,*,#7276,.T.);
#9076=ORIENTED_EDGE('',*,*,#7275,.F.);
#9077=ORIENTED_EDGE('',*,*,#7278,.T.);
#9078=ORIENTED_EDGE('',*,*,#7279,.T.);
#9079=ORIENTED_EDGE('',*,*,#7278,.F.);
#9080=ORIENTED_EDGE('',*,*,#7279,.F.);
#11350=CYLINDRICAL_SURFACE('',#14032,0.35);
#11351=CYLINDRICAL_SURFACE('',#14035,0.2);
#11780=ADVANCED_FACE('',(#2055,#1202),#1574,.F.);
#11781=ADVANCED_FACE('',(#2056),#11350,.T.);
#11782=ADVANCED_FACE('',(#2057),#1575,.T.);
#11783=ADVANCED_FACE('',(#2058),#11351,.T.);
#11784=ADVANCED_FACE('',(#2059),#1576,.F.);
#12411=CLOSED_SHELL('',(#11780,#11781,#11782,#11783,#11784));
#14028=AXIS2_PLACEMENT_3D('',#20511,#16360,#16361);
#14029=AXIS2_PLACEMENT_3D('',#20512,#16362,#16363);
#14030=AXIS2_PLACEMENT_3D('',#20514,#16364,#16365);
#14031=AXIS2_PLACEMENT_3D('',#20516,#16366,#16367);
#14032=AXIS2_PLACEMENT_3D('',#20517,#16368,#16369);
#14033=AXIS2_PLACEMENT_3D('',#20519,#16370,#16371);
#14034=AXIS2_PLACEMENT_3D('',#20521,#16373,#16374);
#14035=AXIS2_PLACEMENT_3D('',#20522,#16375,#16376);
#14036=AXIS2_PLACEMENT_3D('',#20525,#16378,#16379);
#14037=AXIS2_PLACEMENT_3D('',#20526,#16380,#16381);
#16360=DIRECTION('axis',(0.,0.,1.));
#16361=DIRECTION('refdir',(1.,0.,0.));
#16362=DIRECTION('center_axis',(1.,0.,0.));
#16363=DIRECTION('ref_axis',(0.,0.,-1.));
#16364=DIRECTION('center_axis',(1.,0.,0.));
#16365=DIRECTION('ref_axis',(0.,0.,-1.));
#16366=DIRECTION('center_axis',(1.,0.,0.));
#16367=DIRECTION('ref_axis',(0.,0.,-1.));
#16368=DIRECTION('center_axis',(1.,0.,0.));
#16369=DIRECTION('ref_axis',(0.,0.,-1.));
#16370=DIRECTION('center_axis',(1.,0.,0.));
#16371=DIRECTION('ref_axis',(0.,0.,-1.));
#16372=DIRECTION('',(-1.,0.,0.));
#16373=DIRECTION('center_axis',(1.,0.,0.));
#16374=DIRECTION('ref_axis',(0.,0.,-1.));
#16375=DIRECTION('center_axis',(1.,0.,0.));
#16376=DIRECTION('ref_axis',(0.,0.,-1.));
#16377=DIRECTION('',(-1.,0.,0.));
#16378=DIRECTION('center_axis',(1.,0.,0.));
#16379=DIRECTION('ref_axis',(0.,0.,-1.));
#16380=DIRECTION('center_axis',(1.,0.,0.));
#16381=DIRECTION('ref_axis',(0.,0.,-1.));
#20511=CARTESIAN_POINT('',(0.,0.,0.));
#20512=CARTESIAN_POINT('Origin',(-8.8,-4.5,6.15));
#20513=CARTESIAN_POINT('',(-8.8,-4.5,6.5));
#20514=CARTESIAN_POINT('Origin',(-8.8,-4.5,6.15));
#20515=CARTESIAN_POINT('',(-8.8,-4.5,6.35));
#20516=CARTESIAN_POINT('Origin',(-8.8,-4.5,6.15));
#20517=CARTESIAN_POINT('Origin',(-8.8,-4.5,6.15));
#20518=CARTESIAN_POINT('',(-8.4,-4.5,6.5));
#20519=CARTESIAN_POINT('Origin',(-8.4,-4.5,6.15));
#20520=CARTESIAN_POINT('',(-8.8,-4.5,6.5));
#20521=CARTESIAN_POINT('Origin',(-8.4,-4.5,6.15));
#20522=CARTESIAN_POINT('Origin',(-9.5,-4.5,6.15));
#20523=CARTESIAN_POINT('',(-9.5,-4.5,6.35));
#20524=CARTESIAN_POINT('',(-9.5,-4.5,6.35));
#20525=CARTESIAN_POINT('Origin',(-9.5,-4.5,6.15));
#20526=CARTESIAN_POINT('Origin',(-9.5,-4.5,6.15));
#23516=UNCERTAINTY_MEASURE_WITH_UNIT(LENGTH_MEASURE(0.001),#23729,
'DISTANCE_ACCURACY_VALUE',
'Maximum model space distance between geometric entities at asserted c
onnectivities');
#23611=UNCERTAINTY_MEASURE_WITH_UNIT(LENGTH_MEASURE(0.001),#23729,
'DISTANCE_ACCURACY_VALUE',
'Maximum model space distance between geometric entities at asserted c
onnectivities');
#23633=(
GEOMETRIC_REPRESENTATION_CONTEXT(3)
GLOBAL_UNCERTAINTY_ASSIGNED_CONTEXT((#23516))
GLOBAL_UNIT_ASSIGNED_CONTEXT((#23729,#23731,#23732))
REPRESENTATION_CONTEXT('','3D')
);
#23728=(
GEOMETRIC_REPRESENTATION_CONTEXT(3)
GLOBAL_UNCERTAINTY_ASSIGNED_CONTEXT((#23611))
GLOBAL_UNIT_ASSIGNED_CONTEXT((#23729,#23731,#23732))
REPRESENTATION_CONTEXT('','3D')
);
#23729=(
LENGTH_UNIT()
NAMED_UNIT(*)
SI_UNIT(.CENTI.,.METRE.)
);
#23731=(
NAMED_UNIT(*)
PLANE_ANGLE_UNIT()
SI_UNIT($,.RADIAN.)
);
#23732=(
NAMED_UNIT(*)
SI_UNIT($,.STERADIAN.)
SOLID_ANGLE_UNIT()
);
#23754=SHAPE_DEFINITION_REPRESENTATION(#23870,#24133);
#23870=PRODUCT_DEFINITION_SHAPE('',$,#24250);
#24133=SHAPE_REPRESENTATION('',(#14028),#23633);
#24228=PRODUCT_DEFINITION_CONTEXT('part definition',#24578,'design');
#24250=PRODUCT_DEFINITION('Screw keeper fastener (3)',
'Screw keeper fastener (3)',#24366,#24228);
#24366=PRODUCT_DEFINITION_FORMATION('',$,#24601);
#24578=APPLICATION_CONTEXT(
'Core Data for Automotive Mechanical Design Process');
#24579=PRODUCT_CONTEXT('part definition',#24578,'mechanical');
#24601=PRODUCT('Screw keeper fastener (3)','Screw keeper fastener (3)',
'Screw keeper fastener (3)',(#24579));
#24766=COLOUR_RGB('Black',0.12,0.14,0.17);
#24767=FILL_AREA_STYLE_COLOUR('',#24766);
#24768=FILL_AREA_STYLE('',(#24767));
#24769=SURFACE_STYLE_FILL_AREA(#24768);
#24770=SURFACE_SIDE_STYLE('',(#24769));
#24771=SURFACE_STYLE_USAGE(.BOTH.,#24770);
#24772=PRESENTATION_STYLE_ASSIGNMENT((#24771));
ENDSEC;
END-ISO-10303-21;
